ISO-10303-21;
HEADER;
/* Generated by software containing ST-Developer
 * from STEP Tools, Inc. (www.steptools.com) 
 */

FILE_DESCRIPTION(
/* description */ ('Bin tilter linkage'),
/* implementation_level */ '2;1');

FILE_NAME(
/* name */ 'M4 short cap screw (6).step',
/* time_stamp */ '2026-10-28T03:26:24-07:00',
/* author */ (''),
/* organization */ (''),
/* preprocessor_version */ 'ST-DEVELOPER v20.2',
/* originating_system */ 'Autodesk Translation Framework v15.17.0.0',
/* authorisation */ '');

FILE_SCHEMA (('AUTOMOTIVE_DESIGN { 1 0 10303 214 3 1 1 }'));
ENDSEC;

DATA;
#10=MECHANICAL_DESIGN_GEOMETRIC_PRESENTATION_REPRESENTATION('',(#901),#23728);
#689=SHAPE_REPRESENTATION_RELATIONSHIP('SRR','None',#24154,#795);
#795=ADVANCED_BREP_SHAPE_REPRESENTATION('',(#1014),#23654);
#901=STYLED_ITEM('',(#24772),#1014);
#1014=MANIFOLD_SOLID_BREP('Body1',#12432);
#1280=FACE_BOUND('',#3172,.T.);
#1643=PLANE('',#14346);
#1644=PLANE('',#14351);
#1645=PLANE('',#14354);
#2201=FACE_OUTER_BOUND('',#3171,.T.);
#2202=FACE_OUTER_BOUND('',#3173,.T.);
#2203=FACE_OUTER_BOUND('',#3174,.T.);
#2204=FACE_OUTER_BOUND('',#3175,.T.);
#2205=FACE_OUTER_BOUND('',#3176,.T.);
#3171=EDGE_LOOP('',(#9601));
#3172=EDGE_LOOP('',(#9602));
#3173=EDGE_LOOP('',(#9603,#9604,#9605,#9606));
#3174=EDGE_LOOP('',(#9607));
#3175=EDGE_LOOP('',(#9608,#9609,#9610,#9611));
#3176=EDGE_LOOP('',(#9612));
#4147=LINE('',#21129,#4822);
#4148=LINE('',#21133,#4823);
#4822=VECTOR('',#17122,0.35);
#4823=VECTOR('',#17127,0.2);
#5515=CIRCLE('',#14347,0.35);
#5516=CIRCLE('',#14348,0.2);
#5517=CIRCLE('',#14350,0.35);
#5518=CIRCLE('',#14353,0.2);
#6365=VERTEX_POINT('',#21122);
#6366=VERTEX_POINT('',#21124);
#6367=VERTEX_POINT('',#21127);
#6368=VERTEX_POINT('',#21132);
#7540=EDGE_CURVE('',#6365,#6365,#5515,.T.);
#7541=EDGE_CURVE('',#6366,#6366,#5516,.T.);
#7542=EDGE_CURVE('',#6367,#6367,#5517,.T.);
#7543=EDGE_CURVE('',#6367,#6365,#4147,.T.);
#7544=EDGE_CURVE('',#6366,#6368,#4148,.T.);
#7545=EDGE_CURVE('',#6368,#6368,#5518,.T.);
#9601=ORIENTED_EDGE('',*,*,#7540,.F.);
#9602=ORIENTED_EDGE('',*,*,#7541,.T.);
#9603=ORIENTED_EDGE('',*,*,#7542,.F.);
#9604=ORIENTED_EDGE('',*,*,#7543,.T.);
#9605=ORIENTED_EDGE('',*,*,#7540,.T.);
#9606=ORIENTED_EDGE('',*,*,#7543,.F.);
#9607=ORIENTED_EDGE('',*,*,#7542,.T.);
#9608=ORIENTED_EDGE('',*,*,#7541,.F.);
#9609=ORIENTED_EDGE('',*,*,#7544,.T.);
#9610=ORIENTED_EDGE('',*,*,#7545,.T.);
#9611=ORIENTED_EDGE('',*,*,#7544,.F.);
#9612=ORIENTED_EDGE('',*,*,#7545,.F.);
#11423=CYLINDRICAL_SURFACE('',#14349,0.35);
#11424=CYLINDRICAL_SURFACE('',#14352,0.2);
#11926=ADVANCED_FACE('',(#2201,#1280),#1643,.F.);
#11927=ADVANCED_FACE('',(#2202),#11423,.T.);
#11928=ADVANCED_FACE('',(#2203),#1644,.T.);
#11929=ADVANCED_FACE('',(#2204),#11424,.T.);
#11930=ADVANCED_FACE('',(#2205),#1645,.F.);
#12432=CLOSED_SHELL('',(#11926,#11927,#11928,#11929,#11930));
#14345=AXIS2_PLACEMENT_3D('',#21120,#17110,#17111);
#14346=AXIS2_PLACEMENT_3D('',#21121,#17112,#17113);
#14347=AXIS2_PLACEMENT_3D('',#21123,#17114,#17115);
#14348=AXIS2_PLACEMENT_3D('',#21125,#17116,#17117);
#14349=AXIS2_PLACEMENT_3D('',#21126,#17118,#17119);
#14350=AXIS2_PLACEMENT_3D('',#21128,#17120,#17121);
#14351=AXIS2_PLACEMENT_3D('',#21130,#17123,#17124);
#14352=AXIS2_PLACEMENT_3D('',#21131,#17125,#17126);
#14353=AXIS2_PLACEMENT_3D('',#21134,#17128,#17129);
#14354=AXIS2_PLACEMENT_3D('',#21135,#17130,#17131);
#17110=DIRECTION('axis',(0.,0.,1.));
#17111=DIRECTION('refdir',(1.,0.,0.));
#17112=DIRECTION('center_axis',(0.,1.,0.));
#17113=DIRECTION('ref_axis',(1.,0.,0.));
#17114=DIRECTION('center_axis',(0.,1.,0.));
#17115=DIRECTION('ref_axis',(1.,0.,0.));
#17116=DIRECTION('center_axis',(0.,1.,0.));
#17117=DIRECTION('ref_axis',(1.,0.,0.));
#17118=DIRECTION('center_axis',(0.,1.,0.));
#17119=DIRECTION('ref_axis',(1.,0.,0.));
#17120=DIRECTION('center_axis',(0.,1.,0.));
#17121=DIRECTION('ref_axis',(1.,0.,0.));
#17122=DIRECTION('',(0.,-1.,0.));
#17123=DIRECTION('center_axis',(0.,1.,0.));
#17124=DIRECTION('ref_axis',(1.,0.,0.));
#17125=DIRECTION('center_axis',(0.,1.,0.));
#17126=DIRECTION('ref_axis',(1.,0.,0.));
#17127=DIRECTION('',(0.,-1.,0.));
#17128=DIRECTION('center_axis',(0.,1.,0.));
#17129=DIRECTION('ref_axis',(1.,0.,0.));
#17130=DIRECTION('center_axis',(0.,1.,0.));
#17131=DIRECTION('ref_axis',(1.,0.,0.));
#21120=CARTESIAN_POINT('',(0.,0.,0.));
#21121=CARTESIAN_POINT('Origin',(-1.30814754519511,0.8,13.6918524548049));
#21122=CARTESIAN_POINT('',(-1.65814754519511,0.8,13.6918524548049));
#21123=CARTESIAN_POINT('Origin',(-1.30814754519511,0.8,13.6918524548049));
#21124=CARTESIAN_POINT('',(-1.50814754519511,0.8,13.6918524548049));
#21125=CARTESIAN_POINT('Origin',(-1.30814754519511,0.8,13.6918524548049));
#21126=CARTESIAN_POINT('Origin',(-1.30814754519511,0.8,13.6918524548049));
#21127=CARTESIAN_POINT('',(-1.65814754519511,1.2,13.6918524548049));
#21128=CARTESIAN_POINT('Origin',(-1.30814754519511,1.2,13.6918524548049));
#21129=CARTESIAN_POINT('',(-1.65814754519511,0.8,13.6918524548049));
#21130=CARTESIAN_POINT('Origin',(-1.30814754519511,1.2,13.6918524548049));
#21131=CARTESIAN_POINT('Origin',(-1.30814754519511,0.1,13.6918524548049));
#21132=CARTESIAN_POINT('',(-1.50814754519511,0.1,13.6918524548049));
#21133=CARTESIAN_POINT('',(-1.50814754519511,0.1,13.6918524548049));
#21134=CARTESIAN_POINT('Origin',(-1.30814754519511,0.1,13.6918524548049));
#21135=CARTESIAN_POINT('Origin',(-1.30814754519511,0.1,13.6918524548049));
#23537=UNCERTAINTY_MEASURE_WITH_UNIT(LENGTH_MEASURE(0.001),#23729,
'DISTANCE_ACCURACY_VALUE',
'Maximum model space distance between geometric entities at asserted c
onnectivities');
#23611=UNCERTAINTY_MEASURE_WITH_UNIT(LENGTH_MEASURE(0.001),#23729,
'DISTANCE_ACCURACY_VALUE',
'Maximum model space distance between geometric entities at asserted c
onnectivities');
#23654=(
GEOMETRIC_REPRESENTATION_CONTEXT(3)
GLOBAL_UNCERTAINTY_ASSIGNED_CONTEXT((#23537))
GLOBAL_UNIT_ASSIGNED_CONTEXT((#23729,#23731,#23732))
REPRESENTATION_CONTEXT('','3D')
);
#23728=(
GEOMETRIC_REPRESENTATION_CONTEXT(3)
GLOBAL_UNCERTAINTY_ASSIGNED_CONTEXT((#23611))
GLOBAL_UNIT_ASSIGNED_CONTEXT((#23729,#23731,#23732))
REPRESENTATION_CONTEXT('','3D')
);
#23729=(
LENGTH_UNIT()
NAMED_UNIT(*)
SI_UNIT(.CENTI.,.METRE.)
);
#23731=(
NAMED_UNIT(*)
PLANE_ANGLE_UNIT()
SI_UNIT($,.RADIAN.)
);
#23732=(
NAMED_UNIT(*)
SI_UNIT($,.STERADIAN.)
SOLID_ANGLE_UNIT()
);
#23775=SHAPE_DEFINITION_REPRESENTATION(#23891,#24154);
#23891=PRODUCT_DEFINITION_SHAPE('',$,#24271);
#24154=SHAPE_REPRESENTATION('',(#14345),#23654);
#24228=PRODUCT_DEFINITION_CONTEXT('part definition',#24578,'design');
#24271=PRODUCT_DEFINITION('M4 short cap screw (6)',
'M4 short cap screw (6)',#24387,#24228);
#24387=PRODUCT_DEFINITION_FORMATION('',$,#24622);
#24578=APPLICATION_CONTEXT(
'Core Data for Automotive Mechanical Design Process');
#24579=PRODUCT_CONTEXT('part definition',#24578,'mechanical');
#24622=PRODUCT('M4 short cap screw (6)','M4 short cap screw (6)',
'M4 short cap screw (6)',(#24579));
#24766=COLOUR_RGB('Black',0.12,0.14,0.17);
#24767=FILL_AREA_STYLE_COLOUR('',#24766);
#24768=FILL_AREA_STYLE('',(#24767));
#24769=SURFACE_STYLE_FILL_AREA(#24768);
#24770=SURFACE_SIDE_STYLE('',(#24769));
#24771=SURFACE_STYLE_USAGE(.BOTH.,#24770);
#24772=PRESENTATION_STYLE_ASSIGNMENT((#24771));
ENDSEC;
END-ISO-10303-21;
